ISO-10303-21;
HEADER;
/* Generated by software containing ST-Developer
 * from STEP Tools, Inc. (www.steptools.com) 
 */

FILE_DESCRIPTION(
/* description */ ('Hand-crank gear train demonstrator'),
/* implementation_level */ '2;1');

FILE_NAME(
/* name */ 'M6x30 handle bolt.step',
/* time_stamp */ '2026-10-28T03:22:13-07:00',
/* author */ (''),
/* organization */ (''),
/* preprocessor_version */ 'ST-DEVELOPER v20.2',
/* originating_system */ 'Autodesk Translation Framework v15.17.0.0',
/* authorisation */ '');

FILE_SCHEMA (('AUTOMOTIVE_DESIGN { 1 0 10303 214 3 1 1 }'));
ENDSEC;

DATA;
#10=MECHANICAL_DESIGN_GEOMETRIC_PRESENTATION_REPRESENTATION('',(#1242),#62758);
#1042=CONICAL_SURFACE('',#18124,0.475,0.785398163397449);
#1043=CONICAL_SURFACE('',#18128,0.485,0.785398163397448);
#1044=CONICAL_SURFACE('',#18132,0.31,0.463647609000806);
#1054=ORIENTED_CLOSED_SHELL('',*,#16425,.F.);
#1059=BREP_WITH_VOIDS('Body1',#16426,(#1054));
#1099=SHAPE_REPRESENTATION_RELATIONSHIP('SRR','None',#63074,#1163);
#1163=ADVANCED_BREP_SHAPE_REPRESENTATION('',(#1059),#62728);
#1242=STYLED_ITEM('',(#63469),#1059);
#1570=FACE_BOUND('',#3787,.T.);
#1571=FACE_BOUND('',#3795,.T.);
#1925=PLANE('',#18108);
#1926=PLANE('',#18109);
#1927=PLANE('',#18110);
#1928=PLANE('',#18111);
#1929=PLANE('',#18112);
#1930=PLANE('',#18113);
#1931=PLANE('',#18114);
#1932=PLANE('',#18115);
#1933=PLANE('',#18116);
#1934=PLANE('',#18121);
#1935=PLANE('',#18122);
#1936=PLANE('',#18130);
#2614=FACE_OUTER_BOUND('',#3778,.T.);
#2615=FACE_OUTER_BOUND('',#3779,.T.);
#2616=FACE_OUTER_BOUND('',#3780,.T.);
#2617=FACE_OUTER_BOUND('',#3781,.T.);
#2618=FACE_OUTER_BOUND('',#3782,.T.);
#2619=FACE_OUTER_BOUND('',#3783,.T.);
#2620=FACE_OUTER_BOUND('',#3784,.T.);
#2621=FACE_OUTER_BOUND('',#3785,.T.);
#2622=FACE_OUTER_BOUND('',#3786,.T.);
#2623=FACE_OUTER_BOUND('',#3788,.T.);
#2624=FACE_OUTER_BOUND('',#3789,.T.);
#2625=FACE_OUTER_BOUND('',#3790,.T.);
#2626=FACE_OUTER_BOUND('',#3791,.T.);
#2627=FACE_OUTER_BOUND('',#3792,.T.);
#2628=FACE_OUTER_BOUND('',#3793,.T.);
#2629=FACE_OUTER_BOUND('',#3794,.T.);
#2630=FACE_OUTER_BOUND('',#3796,.T.);
#2631=FACE_OUTER_BOUND('',#3797,.T.);
#3778=EDGE_LOOP('',(#12957,#12958,#12959,#12960));
#3779=EDGE_LOOP('',(#12961,#12962,#12963,#12964));
#3780=EDGE_LOOP('',(#12965,#12966,#12967,#12968));
#3781=EDGE_LOOP('',(#12969,#12970,#12971,#12972));
#3782=EDGE_LOOP('',(#12973,#12974,#12975,#12976));
#3783=EDGE_LOOP('',(#12977,#12978,#12979,#12980));
#3784=EDGE_LOOP('',(#12981,#12982,#12983,#12984,#12985,#12986));
#3785=EDGE_LOOP('',(#12987,#12988,#12989,#12990,#12991,#12992));
#3786=EDGE_LOOP('',(#12993));
#3787=EDGE_LOOP('',(#12994));
#3788=EDGE_LOOP('',(#12995,#12996,#12997,#12998));
#3789=EDGE_LOOP('',(#12999));
#3790=EDGE_LOOP('',(#13000));
#3791=EDGE_LOOP('',(#13001,#13002,#13003,#13004));
#3792=EDGE_LOOP('',(#13005,#13006,#13007,#13008));
#3793=EDGE_LOOP('',(#13009,#13010,#13011,#13012));
#3794=EDGE_LOOP('',(#13013));
#3795=EDGE_LOOP('',(#13014));
#3796=EDGE_LOOP('',(#13015,#13016,#13017,#13018));
#3797=EDGE_LOOP('',(#13019,#13020,#13021,#13022));
#4906=LINE('',#26324,#6038);
#4907=LINE('',#26326,#6039);
#4908=LINE('',#26328,#6040);
#4909=LINE('',#26329,#6041);
#4910=LINE('',#26332,#6042);
#4911=LINE('',#26334,#6043);
#4912=LINE('',#26335,#6044);
#4913=LINE('',#26338,#6045);
#4914=LINE('',#26340,#6046);
#4915=LINE('',#26341,#6047);
#4916=LINE('',#26344,#6048);
#4917=LINE('',#26346,#6049);
#4918=LINE('',#26347,#6050);
#4919=LINE('',#26350,#6051);
#4920=LINE('',#26352,#6052);
#4921=LINE('',#26353,#6053);
#4922=LINE('',#26355,#6054);
#4923=LINE('',#26356,#6055);
#4924=LINE('',#26366,#6056);
#4925=LINE('',#26375,#6057);
#4926=LINE('',#26379,#6058);
#4927=LINE('',#26383,#6059);
#4928=LINE('',#26390,#6060);
#4929=LINE('',#26392,#6061);
#6038=VECTOR('',#21353,1.);
#6039=VECTOR('',#21354,1.);
#6040=VECTOR('',#21355,1.);
#6041=VECTOR('',#21356,1.);
#6042=VECTOR('',#21359,1.);
#6043=VECTOR('',#21360,1.);
#6044=VECTOR('',#21361,1.);
#6045=VECTOR('',#21364,1.);
#6046=VECTOR('',#21365,1.);
#6047=VECTOR('',#21366,1.);
#6048=VECTOR('',#21369,1.);
#6049=VECTOR('',#21370,1.);
#6050=VECTOR('',#21371,1.);
#6051=VECTOR('',#21374,1.);
#6052=VECTOR('',#21375,1.);
#6053=VECTOR('',#21376,1.);
#6054=VECTOR('',#21379,1.);
#6055=VECTOR('',#21380,1.);
#6056=VECTOR('',#21393,0.3);
#6057=VECTOR('',#21406,0.475);
#6058=VECTOR('',#21411,0.5);
#6059=VECTOR('',#21416,0.485);
#6060=VECTOR('',#21425,0.31);
#6061=VECTOR('',#21428,0.3);
#6955=CIRCLE('',#18117,0.3);
#6956=CIRCLE('',#18118,0.2942);
#6957=CIRCLE('',#18120,0.3);
#6958=CIRCLE('',#18123,0.45);
#6959=CIRCLE('',#18125,0.5);
#6960=CIRCLE('',#18127,0.5);
#6961=CIRCLE('',#18129,0.47);
#6962=CIRCLE('',#18131,0.32);
#6963=CIRCLE('',#18133,0.2942);
#7934=VERTEX_POINT('',#26322);
#7935=VERTEX_POINT('',#26323);
#7936=VERTEX_POINT('',#26325);
#7937=VERTEX_POINT('',#26327);
#7938=VERTEX_POINT('',#26331);
#7939=VERTEX_POINT('',#26333);
#7940=VERTEX_POINT('',#26337);
#7941=VERTEX_POINT('',#26339);
#7942=VERTEX_POINT('',#26343);
#7943=VERTEX_POINT('',#26345);
#7944=VERTEX_POINT('',#26349);
#7945=VERTEX_POINT('',#26351);
#7946=VERTEX_POINT('',#26360);
#7947=VERTEX_POINT('',#26362);
#7948=VERTEX_POINT('',#26365);
#7949=VERTEX_POINT('',#26370);
#7950=VERTEX_POINT('',#26373);
#7951=VERTEX_POINT('',#26377);
#7952=VERTEX_POINT('',#26381);
#7953=VERTEX_POINT('',#26385);
#7954=VERTEX_POINT('',#26388);
#9730=EDGE_CURVE('',#7934,#7935,#4906,.T.);
#9731=EDGE_CURVE('',#7935,#7936,#4907,.T.);
#9732=EDGE_CURVE('',#7936,#7937,#4908,.T.);
#9733=EDGE_CURVE('',#7934,#7937,#4909,.T.);
#9734=EDGE_CURVE('',#7935,#7938,#4910,.T.);
#9735=EDGE_CURVE('',#7938,#7939,#4911,.T.);
#9736=EDGE_CURVE('',#7939,#7936,#4912,.T.);
#9737=EDGE_CURVE('',#7938,#7940,#4913,.T.);
#9738=EDGE_CURVE('',#7940,#7941,#4914,.T.);
#9739=EDGE_CURVE('',#7941,#7939,#4915,.T.);
#9740=EDGE_CURVE('',#7940,#7942,#4916,.T.);
#9741=EDGE_CURVE('',#7942,#7943,#4917,.T.);
#9742=EDGE_CURVE('',#7943,#7941,#4918,.T.);
#9743=EDGE_CURVE('',#7942,#7944,#4919,.T.);
#9744=EDGE_CURVE('',#7944,#7945,#4920,.T.);
#9745=EDGE_CURVE('',#7945,#7943,#4921,.T.);
#9746=EDGE_CURVE('',#7944,#7934,#4922,.T.);
#9747=EDGE_CURVE('',#7937,#7945,#4923,.T.);
#9748=EDGE_CURVE('',#7946,#7946,#6955,.T.);
#9749=EDGE_CURVE('',#7947,#7947,#6956,.T.);
#9750=EDGE_CURVE('',#7946,#7948,#4924,.T.);
#9751=EDGE_CURVE('',#7948,#7948,#6957,.T.);
#9752=EDGE_CURVE('',#7949,#7949,#6958,.T.);
#9753=EDGE_CURVE('',#7950,#7950,#6959,.T.);
#9754=EDGE_CURVE('',#7950,#7949,#4925,.T.);
#9755=EDGE_CURVE('',#7951,#7951,#6960,.T.);
#9756=EDGE_CURVE('',#7951,#7950,#4926,.T.);
#9757=EDGE_CURVE('',#7952,#7952,#6961,.T.);
#9758=EDGE_CURVE('',#7952,#7951,#4927,.T.);
#9759=EDGE_CURVE('',#7953,#7953,#6962,.T.);
#9760=EDGE_CURVE('',#7954,#7954,#6963,.F.);
#9761=EDGE_CURVE('',#7954,#7953,#4928,.T.);
#9762=EDGE_CURVE('',#7947,#7954,#4929,.T.);
#12957=ORIENTED_EDGE('',*,*,#9730,.T.);
#12958=ORIENTED_EDGE('',*,*,#9731,.T.);
#12959=ORIENTED_EDGE('',*,*,#9732,.T.);
#12960=ORIENTED_EDGE('',*,*,#9733,.F.);
#12961=ORIENTED_EDGE('',*,*,#9734,.T.);
#12962=ORIENTED_EDGE('',*,*,#9735,.T.);
#12963=ORIENTED_EDGE('',*,*,#9736,.T.);
#12964=ORIENTED_EDGE('',*,*,#9731,.F.);
#12965=ORIENTED_EDGE('',*,*,#9737,.T.);
#12966=ORIENTED_EDGE('',*,*,#9738,.T.);
#12967=ORIENTED_EDGE('',*,*,#9739,.T.);
#12968=ORIENTED_EDGE('',*,*,#9735,.F.);
#12969=ORIENTED_EDGE('',*,*,#9740,.T.);
#12970=ORIENTED_EDGE('',*,*,#9741,.T.);
#12971=ORIENTED_EDGE('',*,*,#9742,.T.);
#12972=ORIENTED_EDGE('',*,*,#9738,.F.);
#12973=ORIENTED_EDGE('',*,*,#9743,.T.);
#12974=ORIENTED_EDGE('',*,*,#9744,.T.);
#12975=ORIENTED_EDGE('',*,*,#9745,.T.);
#12976=ORIENTED_EDGE('',*,*,#9741,.F.);
#12977=ORIENTED_EDGE('',*,*,#9746,.T.);
#12978=ORIENTED_EDGE('',*,*,#9733,.T.);
#12979=ORIENTED_EDGE('',*,*,#9747,.T.);
#12980=ORIENTED_EDGE('',*,*,#9744,.F.);
#12981=ORIENTED_EDGE('',*,*,#9746,.F.);
#12982=ORIENTED_EDGE('',*,*,#9743,.F.);
#12983=ORIENTED_EDGE('',*,*,#9740,.F.);
#12984=ORIENTED_EDGE('',*,*,#9737,.F.);
#12985=ORIENTED_EDGE('',*,*,#9734,.F.);
#12986=ORIENTED_EDGE('',*,*,#9730,.F.);
#12987=ORIENTED_EDGE('',*,*,#9747,.F.);
#12988=ORIENTED_EDGE('',*,*,#9732,.F.);
#12989=ORIENTED_EDGE('',*,*,#9736,.F.);
#12990=ORIENTED_EDGE('',*,*,#9739,.F.);
#12991=ORIENTED_EDGE('',*,*,#9742,.F.);
#12992=ORIENTED_EDGE('',*,*,#9745,.F.);
#12993=ORIENTED_EDGE('',*,*,#9748,.T.);
#12994=ORIENTED_EDGE('',*,*,#9749,.F.);
#12995=ORIENTED_EDGE('',*,*,#9748,.F.);
#12996=ORIENTED_EDGE('',*,*,#9750,.T.);
#12997=ORIENTED_EDGE('',*,*,#9751,.T.);
#12998=ORIENTED_EDGE('',*,*,#9750,.F.);
#12999=ORIENTED_EDGE('',*,*,#9751,.F.);
#13000=ORIENTED_EDGE('',*,*,#9752,.F.);
#13001=ORIENTED_EDGE('',*,*,#9753,.F.);
#13002=ORIENTED_EDGE('',*,*,#9754,.T.);
#13003=ORIENTED_EDGE('',*,*,#9752,.T.);
#13004=ORIENTED_EDGE('',*,*,#9754,.F.);
#13005=ORIENTED_EDGE('',*,*,#9755,.F.);
#13006=ORIENTED_EDGE('',*,*,#9756,.T.);
#13007=ORIENTED_EDGE('',*,*,#9753,.T.);
#13008=ORIENTED_EDGE('',*,*,#9756,.F.);
#13009=ORIENTED_EDGE('',*,*,#9757,.F.);
#13010=ORIENTED_EDGE('',*,*,#9758,.T.);
#13011=ORIENTED_EDGE('',*,*,#9755,.T.);
#13012=ORIENTED_EDGE('',*,*,#9758,.F.);
#13013=ORIENTED_EDGE('',*,*,#9757,.T.);
#13014=ORIENTED_EDGE('',*,*,#9759,.F.);
#13015=ORIENTED_EDGE('',*,*,#9760,.F.);
#13016=ORIENTED_EDGE('',*,*,#9761,.T.);
#13017=ORIENTED_EDGE('',*,*,#9759,.T.);
#13018=ORIENTED_EDGE('',*,*,#9761,.F.);
#13019=ORIENTED_EDGE('',*,*,#9749,.T.);
#13020=ORIENTED_EDGE('',*,*,#9762,.T.);
#13021=ORIENTED_EDGE('',*,*,#9760,.T.);
#13022=ORIENTED_EDGE('',*,*,#9762,.F.);
#15315=CYLINDRICAL_SURFACE('',#18119,0.3);
#15316=CYLINDRICAL_SURFACE('',#18126,0.5);
#15317=CYLINDRICAL_SURFACE('',#18134,0.2942);
#15924=ADVANCED_FACE('',(#2614),#1925,.F.);
#15925=ADVANCED_FACE('',(#2615),#1926,.F.);
#15926=ADVANCED_FACE('',(#2616),#1927,.F.);
#15927=ADVANCED_FACE('',(#2617),#1928,.F.);
#15928=ADVANCED_FACE('',(#2618),#1929,.F.);
#15929=ADVANCED_FACE('',(#2619),#1930,.F.);
#15930=ADVANCED_FACE('',(#2620),#1931,.F.);
#15931=ADVANCED_FACE('',(#2621),#1932,.F.);
#15932=ADVANCED_FACE('',(#2622,#1570),#1933,.T.);
#15933=ADVANCED_FACE('',(#2623),#15315,.T.);
#15934=ADVANCED_FACE('',(#2624),#1934,.F.);
#15935=ADVANCED_FACE('',(#2625),#1935,.T.);
#15936=ADVANCED_FACE('',(#2626),#1042,.T.);
#15937=ADVANCED_FACE('',(#2627),#15316,.T.);
#15938=ADVANCED_FACE('',(#2628),#1043,.T.);
#15939=ADVANCED_FACE('',(#2629,#1571),#1936,.T.);
#15940=ADVANCED_FACE('',(#2630),#1044,.T.);
#15941=ADVANCED_FACE('',(#2631),#15317,.T.);
#16425=CLOSED_SHELL('',(#15924,#15925,#15926,#15927,#15928,#15929,#15930,
#15931));
#16426=CLOSED_SHELL('',(#15932,#15933,#15934,#15935,#15936,#15937,#15938,
#15939,#15940,#15941));
#18107=AXIS2_PLACEMENT_3D('',#26320,#21349,#21350);
#18108=AXIS2_PLACEMENT_3D('',#26321,#21351,#21352);
#18109=AXIS2_PLACEMENT_3D('',#26330,#21357,#21358);
#18110=AXIS2_PLACEMENT_3D('',#26336,#21362,#21363);
#18111=AXIS2_PLACEMENT_3D('',#26342,#21367,#21368);
#18112=AXIS2_PLACEMENT_3D('',#26348,#21372,#21373);
#18113=AXIS2_PLACEMENT_3D('',#26354,#21377,#21378);
#18114=AXIS2_PLACEMENT_3D('',#26357,#21381,#21382);
#18115=AXIS2_PLACEMENT_3D('',#26358,#21383,#21384);
#18116=AXIS2_PLACEMENT_3D('',#26359,#21385,#21386);
#18117=AXIS2_PLACEMENT_3D('',#26361,#21387,#21388);
#18118=AXIS2_PLACEMENT_3D('',#26363,#21389,#21390);
#18119=AXIS2_PLACEMENT_3D('',#26364,#21391,#21392);
#18120=AXIS2_PLACEMENT_3D('',#26367,#21394,#21395);
#18121=AXIS2_PLACEMENT_3D('',#26368,#21396,#21397);
#18122=AXIS2_PLACEMENT_3D('',#26369,#21398,#21399);
#18123=AXIS2_PLACEMENT_3D('',#26371,#21400,#21401);
#18124=AXIS2_PLACEMENT_3D('',#26372,#21402,#21403);
#18125=AXIS2_PLACEMENT_3D('',#26374,#21404,#21405);
#18126=AXIS2_PLACEMENT_3D('',#26376,#21407,#21408);
#18127=AXIS2_PLACEMENT_3D('',#26378,#21409,#21410);
#18128=AXIS2_PLACEMENT_3D('',#26380,#21412,#21413);
#18129=AXIS2_PLACEMENT_3D('',#26382,#21414,#21415);
#18130=AXIS2_PLACEMENT_3D('',#26384,#21417,#21418);
#18131=AXIS2_PLACEMENT_3D('',#26386,#21419,#21420);
#18132=AXIS2_PLACEMENT_3D('',#26387,#21421,#21422);
#18133=AXIS2_PLACEMENT_3D('',#26389,#21423,#21424);
#18134=AXIS2_PLACEMENT_3D('',#26391,#21426,#21427);
#21349=DIRECTION('axis',(0.,0.,1.));
#21350=DIRECTION('refdir',(1.,0.,0.));
#21351=DIRECTION('center_axis',(0.866025403784439,0.,-0.5));
#21352=DIRECTION('ref_axis',(0.5,0.,0.866025403784439));
#21353=DIRECTION('',(-0.5,0.,-0.866025403784439));
#21354=DIRECTION('',(0.,-1.,0.));
#21355=DIRECTION('',(0.5,0.,0.866025403784439));
#21356=DIRECTION('',(0.,-1.,0.));
#21357=DIRECTION('center_axis',(1.92296268638356E-16,0.,-1.));
#21358=DIRECTION('ref_axis',(1.,0.,1.92296268638356E-16));
#21359=DIRECTION('',(-1.,0.,-1.92296268638356E-16));
#21360=DIRECTION('',(0.,-1.,0.));
#21361=DIRECTION('',(1.,0.,1.92296268638356E-16));
#21362=DIRECTION('center_axis',(-0.866025403784439,0.,-0.5));
#21363=DIRECTION('ref_axis',(0.5,0.,-0.866025403784439));
#21364=DIRECTION('',(-0.5,0.,0.866025403784438));
#21365=DIRECTION('',(0.,-1.,0.));
#21366=DIRECTION('',(0.5,0.,-0.866025403784438));
#21367=DIRECTION('center_axis',(-0.866025403784439,0.,0.5));
#21368=DIRECTION('ref_axis',(-0.5,0.,-0.866025403784439));
#21369=DIRECTION('',(0.5,0.,0.866025403784439));
#21370=DIRECTION('',(0.,-1.,0.));
#21371=DIRECTION('',(-0.5,0.,-0.866025403784439));
#21372=DIRECTION('center_axis',(-1.92296268638356E-16,0.,1.));
#21373=DIRECTION('ref_axis',(-1.,0.,-1.92296268638356E-16));
#21374=DIRECTION('',(1.,0.,1.92296268638356E-16));
#21375=DIRECTION('',(0.,-1.,0.));
#21376=DIRECTION('',(-1.,0.,-1.92296268638356E-16));
#21377=DIRECTION('center_axis',(0.866025403784439,0.,0.5));
#21378=DIRECTION('ref_axis',(-0.5,0.,0.866025403784439));
#21379=DIRECTION('',(0.5,0.,-0.866025403784439));
#21380=DIRECTION('',(-0.5,0.,0.866025403784439));
#21381=DIRECTION('center_axis',(0.,1.,0.));
#21382=DIRECTION('ref_axis',(1.,0.,0.));
#21383=DIRECTION('center_axis',(0.,-1.,0.));
#21384=DIRECTION('ref_axis',(0.,0.,-1.));
#21385=DIRECTION('center_axis',(0.,1.,0.));
#21386=DIRECTION('ref_axis',(1.,0.,0.));
#21387=DIRECTION('center_axis',(0.,1.,0.));
#21388=DIRECTION('ref_axis',(1.,0.,0.));
#21389=DIRECTION('center_axis',(0.,1.,0.));
#21390=DIRECTION('ref_axis',(1.,0.,0.));
#21391=DIRECTION('center_axis',(0.,1.,0.));
#21392=DIRECTION('ref_axis',(1.,0.,0.));
#21393=DIRECTION('',(0.,-1.,0.));
#21394=DIRECTION('center_axis',(0.,1.,0.));
#21395=DIRECTION('ref_axis',(1.,0.,0.));
#21396=DIRECTION('center_axis',(0.,1.,0.));
#21397=DIRECTION('ref_axis',(1.,0.,0.));
#21398=DIRECTION('center_axis',(0.,1.,0.));
#21399=DIRECTION('ref_axis',(0.,0.,1.));
#21400=DIRECTION('center_axis',(0.,-1.,0.));
#21401=DIRECTION('ref_axis',(1.,0.,0.));
#21402=DIRECTION('center_axis',(0.,-1.,0.));
#21403=DIRECTION('ref_axis',(1.,0.,0.));
#21404=DIRECTION('center_axis',(0.,-1.,0.));
#21405=DIRECTION('ref_axis',(1.,0.,0.));
#21406=DIRECTION('',(0.707106781186548,0.707106781186547,8.65956056235494E-17));
#21407=DIRECTION('center_axis',(0.,-1.,0.));
#21408=DIRECTION('ref_axis',(1.,0.,0.));
#21409=DIRECTION('center_axis',(0.,-1.,0.));
#21410=DIRECTION('ref_axis',(1.,0.,0.));
#21411=DIRECTION('',(0.,1.,0.));
#21412=DIRECTION('center_axis',(0.,1.,0.));
#21413=DIRECTION('ref_axis',(1.,0.,0.));
#21414=DIRECTION('center_axis',(0.,-1.,0.));
#21415=DIRECTION('ref_axis',(1.,0.,0.));
#21416=DIRECTION('',(-0.707106781186547,0.707106781186548,-8.65956056235493E-17));
#21417=DIRECTION('center_axis',(0.,-1.,0.));
#21418=DIRECTION('ref_axis',(0.,0.,-1.));
#21419=DIRECTION('center_axis',(0.,-1.,0.));
#21420=DIRECTION('ref_axis',(1.,0.,0.));
#21421=DIRECTION('center_axis',(0.,1.,0.));
#21422=DIRECTION('ref_axis',(1.,0.,0.));
#21423=DIRECTION('center_axis',(0.,1.,0.));
#21424=DIRECTION('ref_axis',(1.,0.,0.));
#21425=DIRECTION('',(-0.447213595499958,0.894427190999916,-5.47678698264203E-17));
#21426=DIRECTION('center_axis',(0.,-1.,0.));
#21427=DIRECTION('ref_axis',(1.,0.,0.));
#21428=DIRECTION('',(0.,1.,0.));
#26320=CARTESIAN_POINT('',(0.,0.,0.));
#26321=CARTESIAN_POINT('Origin',(0.144337567297406,-0.6,-0.25));
#26322=CARTESIAN_POINT('',(0.288675134594813,-0.6,0.));
#26323=CARTESIAN_POINT('',(0.144337567297406,-0.6,-0.25));
#26324=CARTESIAN_POINT('',(0.288675134594813,-0.6,0.));
#26325=CARTESIAN_POINT('',(0.144337567297406,-0.96,-0.25));
#26326=CARTESIAN_POINT('',(0.144337567297406,-0.6,-0.25));
#26327=CARTESIAN_POINT('',(0.288675134594813,-0.96,0.));
#26328=CARTESIAN_POINT('',(0.288675134594813,-0.96,0.));
#26329=CARTESIAN_POINT('',(0.288675134594813,-0.6,0.));
#26330=CARTESIAN_POINT('Origin',(-0.144337567297406,-0.6,-0.25));
#26331=CARTESIAN_POINT('',(-0.144337567297406,-0.6,-0.25));
#26332=CARTESIAN_POINT('',(0.144337567297406,-0.6,-0.25));
#26333=CARTESIAN_POINT('',(-0.144337567297406,-0.96,-0.25));
#26334=CARTESIAN_POINT('',(-0.144337567297406,-0.6,-0.25));
#26335=CARTESIAN_POINT('',(0.144337567297406,-0.96,-0.25));
#26336=CARTESIAN_POINT('Origin',(-0.288675134594813,-0.6,-8.32667268468867E-17));
#26337=CARTESIAN_POINT('',(-0.288675134594813,-0.6,-3.53525079574969E-17));
#26338=CARTESIAN_POINT('',(-0.144337567297406,-0.6,-0.25));
#26339=CARTESIAN_POINT('',(-0.288675134594813,-0.96,-5.55111512312578E-17));
#26340=CARTESIAN_POINT('',(-0.288675134594813,-0.6,-3.53525079574969E-17));
#26341=CARTESIAN_POINT('',(-0.144337567297406,-0.96,-0.25));
#26342=CARTESIAN_POINT('Origin',(-0.144337567297407,-0.6,0.25));
#26343=CARTESIAN_POINT('',(-0.144337567297407,-0.6,0.25));
#26344=CARTESIAN_POINT('',(-0.288675134594813,-0.6,-3.53525079574969E-17));
#26345=CARTESIAN_POINT('',(-0.144337567297407,-0.96,0.25));
#26346=CARTESIAN_POINT('',(-0.144337567297407,-0.6,0.25));
#26347=CARTESIAN_POINT('',(-0.288675134594813,-0.96,-3.53525079574969E-17));
#26348=CARTESIAN_POINT('Origin',(0.144337567297406,-0.6,0.25));
#26349=CARTESIAN_POINT('',(0.144337567297406,-0.6,0.25));
#26350=CARTESIAN_POINT('',(-0.144337567297407,-0.6,0.25));
#26351=CARTESIAN_POINT('',(0.144337567297406,-0.96,0.25));
#26352=CARTESIAN_POINT('',(0.144337567297406,-0.6,0.25));
#26353=CARTESIAN_POINT('',(-0.144337567297407,-0.96,0.25));
#26354=CARTESIAN_POINT('Origin',(0.288675134594813,-0.6,0.));
#26355=CARTESIAN_POINT('',(0.144337567297406,-0.6,0.25));
#26356=CARTESIAN_POINT('',(0.144337567297406,-0.96,0.25));
#26357=CARTESIAN_POINT('Origin',(0.,-0.6,0.));
#26358=CARTESIAN_POINT('Origin',(0.,-0.96,0.));
#26359=CARTESIAN_POINT('Origin',(0.,-2.4,0.));
#26360=CARTESIAN_POINT('',(-0.3,-2.4,3.67394039744206E-17));
#26361=CARTESIAN_POINT('Origin',(0.,-2.4,0.));
#26362=CARTESIAN_POINT('',(-0.2942,-2.4,3.60291088309151E-17));
#26363=CARTESIAN_POINT('Origin',(0.,-2.4,0.));
#26364=CARTESIAN_POINT('Origin',(0.,-3.,0.));
#26365=CARTESIAN_POINT('',(-0.3,-3.,3.67394039744206E-17));
#26366=CARTESIAN_POINT('',(-0.3,-3.,3.67394039744206E-17));
#26367=CARTESIAN_POINT('Origin',(0.,-3.,0.));
#26368=CARTESIAN_POINT('Origin',(0.,-3.,0.));
#26369=CARTESIAN_POINT('Origin',(0.45,0.6,0.));
#26370=CARTESIAN_POINT('',(-0.45,0.6,-5.51091059616309E-17));
#26371=CARTESIAN_POINT('Origin',(0.,0.6,0.));
#26372=CARTESIAN_POINT('Origin',(0.,0.575,0.));
#26373=CARTESIAN_POINT('',(-0.5,0.55,-6.12323399573677E-17));
#26374=CARTESIAN_POINT('Origin',(0.,0.55,0.));
#26375=CARTESIAN_POINT('',(-0.475,0.575,-5.81707229594993E-17));
#26376=CARTESIAN_POINT('Origin',(0.,0.29,0.));
#26377=CARTESIAN_POINT('',(-0.5,0.0299999999999998,-6.12323399573677E-17));
#26378=CARTESIAN_POINT('Origin',(0.,0.0299999999999998,0.));
#26379=CARTESIAN_POINT('',(-0.5,0.29,-6.12323399573677E-17));
#26380=CARTESIAN_POINT('Origin',(0.,0.0150000000000001,0.));
#26381=CARTESIAN_POINT('',(-0.47,7.11236625150491E-17,-5.75583995599256E-17));
#26382=CARTESIAN_POINT('Origin',(0.,0.,0.));
#26383=CARTESIAN_POINT('',(-0.485,0.0150000000000001,-5.93953697586466E-17));
#26384=CARTESIAN_POINT('Origin',(0.32,0.,0.));
#26385=CARTESIAN_POINT('',(-0.32,-6.93889390390723E-18,-3.91886975727153E-17));
#26386=CARTESIAN_POINT('Origin',(0.,0.,0.));
#26387=CARTESIAN_POINT('Origin',(0.,-0.02,0.));
#26388=CARTESIAN_POINT('',(-0.2942,-0.0515999999999999,3.60291088309151E-17));
#26389=CARTESIAN_POINT('Origin',(0.,-0.0515999999999999,0.));
#26390=CARTESIAN_POINT('',(-0.31,-0.02,-3.7964050773568E-17));
#26391=CARTESIAN_POINT('Origin',(0.,-1.24,0.));
#26392=CARTESIAN_POINT('',(-0.2942,-1.24,-3.60291088309151E-17));
#62654=UNCERTAINTY_MEASURE_WITH_UNIT(LENGTH_MEASURE(0.001),#62759,
'DISTANCE_ACCURACY_VALUE',
'Maximum model space distance between geometric entities at asserted c
onnectivities');
#62684=UNCERTAINTY_MEASURE_WITH_UNIT(LENGTH_MEASURE(0.001),#62759,
'DISTANCE_ACCURACY_VALUE',
'Maximum model space distance between geometric entities at asserted c
onnectivities');
#62728=(
GEOMETRIC_REPRESENTATION_CONTEXT(3)
GLOBAL_UNCERTAINTY_ASSIGNED_CONTEXT((#62654))
GLOBAL_UNIT_ASSIGNED_CONTEXT((#62759,#62761,#62762))
REPRESENTATION_CONTEXT('','3D')
);
#62758=(
GEOMETRIC_REPRESENTATION_CONTEXT(3)
GLOBAL_UNCERTAINTY_ASSIGNED_CONTEXT((#62684))
GLOBAL_UNIT_ASSIGNED_CONTEXT((#62759,#62761,#62762))
REPRESENTATION_CONTEXT('','3D')
);
#62759=(
LENGTH_UNIT()
NAMED_UNIT(*)
SI_UNIT(.CENTI.,.METRE.)
);
#62761=(
NAMED_UNIT(*)
PLANE_ANGLE_UNIT()
SI_UNIT($,.RADIAN.)
);
#62762=(
NAMED_UNIT(*)
SI_UNIT($,.STERADIAN.)
SOLID_ANGLE_UNIT()
);
#62806=SHAPE_DEFINITION_REPRESENTATION(#62889,#63074);
#62889=PRODUCT_DEFINITION_SHAPE('',$,#63148);
#63074=SHAPE_REPRESENTATION('',(#18107),#62728);
#63104=PRODUCT_DEFINITION_CONTEXT('part definition',#63325,'design');
#63148=PRODUCT_DEFINITION('M6x30 handle bolt','M6x30 handle bolt',#63221,
#63104);
#63221=PRODUCT_DEFINITION_FORMATION('',$,#63370);
#63325=APPLICATION_CONTEXT(
'Core Data for Automotive Mechanical Design Process');
#63326=PRODUCT_CONTEXT('part definition',#63325,'mechanical');
#63370=PRODUCT('M6x30 handle bolt','M6x30 handle bolt',
'M6x30 handle bolt',(#63326));
#63463=COLOUR_RGB('Black',0.12,0.14,0.17);
#63464=FILL_AREA_STYLE_COLOUR('',#63463);
#63465=FILL_AREA_STYLE('',(#63464));
#63466=SURFACE_STYLE_FILL_AREA(#63465);
#63467=SURFACE_SIDE_STYLE('',(#63466));
#63468=SURFACE_STYLE_USAGE(.BOTH.,#63467);
#63469=PRESENTATION_STYLE_ASSIGNMENT((#63468));
ENDSEC;
END-ISO-10303-21;
